ISO-10303-21;
HEADER;
/* Generated by software containing ST-Developer
 * from STEP Tools, Inc. (www.steptools.com) 
 */

FILE_DESCRIPTION(
/* description */ ('Four-bar parallelogram arm'),
/* implementation_level */ '2;1');

FILE_NAME(
/* name */ 'Foot strip (1).step',
/* time_stamp */ '2026-10-28T03:24:55-07:00',
/* author */ (''),
/* organization */ (''),
/* preprocessor_version */ 'ST-DEVELOPER v20.2',
/* originating_system */ 'Autodesk Translation Framework v15.17.0.0',
/* authorisation */ '');

FILE_SCHEMA (('AUTOMOTIVE_DESIGN { 1 0 10303 214 3 1 1 }'));
ENDSEC;

DATA;
#10=MECHANICAL_DESIGN_GEOMETRIC_PRESENTATION_REPRESENTATION('',(#624),#14512);
#524=SHAPE_REPRESENTATION_RELATIONSHIP('SRR','None',#14745,#574);
#574=ADVANCED_BREP_SHAPE_REPRESENTATION('',(#682),#14460);
#624=STYLED_ITEM('',(#15073),#682);
#682=MANIFOLD_SOLID_BREP('Body1',#7328);
#1018=PLANE('',#7967);
#1019=PLANE('',#7968);
#1020=PLANE('',#7969);
#1021=PLANE('',#7970);
#1022=PLANE('',#7971);
#1023=PLANE('',#7972);
#1217=FACE_OUTER_BOUND('',#1645,.T.);
#1218=FACE_OUTER_BOUND('',#1646,.T.);
#1219=FACE_OUTER_BOUND('',#1647,.T.);
#1220=FACE_OUTER_BOUND('',#1648,.T.);
#1221=FACE_OUTER_BOUND('',#1649,.T.);
#1222=FACE_OUTER_BOUND('',#1650,.T.);
#1645=EDGE_LOOP('',(#5060,#5061,#5062,#5063));
#1646=EDGE_LOOP('',(#5064,#5065,#5066,#5067));
#1647=EDGE_LOOP('',(#5068,#5069,#5070,#5071));
#1648=EDGE_LOOP('',(#5072,#5073,#5074,#5075));
#1649=EDGE_LOOP('',(#5076,#5077,#5078,#5079));
#1650=EDGE_LOOP('',(#5080,#5081,#5082,#5083));
#2340=LINE('',#11512,#2734);
#2341=LINE('',#11514,#2735);
#2342=LINE('',#11516,#2736);
#2343=LINE('',#11517,#2737);
#2344=LINE('',#11520,#2738);
#2345=LINE('',#11522,#2739);
#2346=LINE('',#11523,#2740);
#2347=LINE('',#11526,#2741);
#2348=LINE('',#11528,#2742);
#2349=LINE('',#11529,#2743);
#2350=LINE('',#11531,#2744);
#2351=LINE('',#11532,#2745);
#2734=VECTOR('',#9058,1.);
#2735=VECTOR('',#9059,1.);
#2736=VECTOR('',#9060,1.);
#2737=VECTOR('',#9061,1.);
#2738=VECTOR('',#9064,1.);
#2739=VECTOR('',#9065,1.);
#2740=VECTOR('',#9066,1.);
#2741=VECTOR('',#9069,1.);
#2742=VECTOR('',#9070,1.);
#2743=VECTOR('',#9071,1.);
#2744=VECTOR('',#9074,1.);
#2745=VECTOR('',#9075,1.);
#3569=VERTEX_POINT('',#11510);
#3570=VERTEX_POINT('',#11511);
#3571=VERTEX_POINT('',#11513);
#3572=VERTEX_POINT('',#11515);
#3573=VERTEX_POINT('',#11519);
#3574=VERTEX_POINT('',#11521);
#3575=VERTEX_POINT('',#11525);
#3576=VERTEX_POINT('',#11527);
#4161=EDGE_CURVE('',#3569,#3570,#2340,.T.);
#4162=EDGE_CURVE('',#3570,#3571,#2341,.T.);
#4163=EDGE_CURVE('',#3572,#3571,#2342,.T.);
#4164=EDGE_CURVE('',#3569,#3572,#2343,.T.);
#4165=EDGE_CURVE('',#3573,#3569,#2344,.T.);
#4166=EDGE_CURVE('',#3574,#3572,#2345,.T.);
#4167=EDGE_CURVE('',#3573,#3574,#2346,.T.);
#4168=EDGE_CURVE('',#3575,#3573,#2347,.T.);
#4169=EDGE_CURVE('',#3576,#3574,#2348,.T.);
#4170=EDGE_CURVE('',#3575,#3576,#2349,.T.);
#4171=EDGE_CURVE('',#3570,#3575,#2350,.T.);
#4172=EDGE_CURVE('',#3571,#3576,#2351,.T.);
#5060=ORIENTED_EDGE('',*,*,#4161,.T.);
#5061=ORIENTED_EDGE('',*,*,#4162,.T.);
#5062=ORIENTED_EDGE('',*,*,#4163,.F.);
#5063=ORIENTED_EDGE('',*,*,#4164,.F.);
#5064=ORIENTED_EDGE('',*,*,#4165,.T.);
#5065=ORIENTED_EDGE('',*,*,#4164,.T.);
#5066=ORIENTED_EDGE('',*,*,#4166,.F.);
#5067=ORIENTED_EDGE('',*,*,#4167,.F.);
#5068=ORIENTED_EDGE('',*,*,#4168,.T.);
#5069=ORIENTED_EDGE('',*,*,#4167,.T.);
#5070=ORIENTED_EDGE('',*,*,#4169,.F.);
#5071=ORIENTED_EDGE('',*,*,#4170,.F.);
#5072=ORIENTED_EDGE('',*,*,#4171,.T.);
#5073=ORIENTED_EDGE('',*,*,#4170,.T.);
#5074=ORIENTED_EDGE('',*,*,#4172,.F.);
#5075=ORIENTED_EDGE('',*,*,#4162,.F.);
#5076=ORIENTED_EDGE('',*,*,#4172,.T.);
#5077=ORIENTED_EDGE('',*,*,#4169,.T.);
#5078=ORIENTED_EDGE('',*,*,#4166,.T.);
#5079=ORIENTED_EDGE('',*,*,#4163,.T.);
#5080=ORIENTED_EDGE('',*,*,#4171,.F.);
#5081=ORIENTED_EDGE('',*,*,#4161,.F.);
#5082=ORIENTED_EDGE('',*,*,#4165,.F.);
#5083=ORIENTED_EDGE('',*,*,#4168,.F.);
#6922=ADVANCED_FACE('',(#1217),#1018,.T.);
#6923=ADVANCED_FACE('',(#1218),#1019,.T.);
#6924=ADVANCED_FACE('',(#1219),#1020,.T.);
#6925=ADVANCED_FACE('',(#1220),#1021,.T.);
#6926=ADVANCED_FACE('',(#1221),#1022,.T.);
#6927=ADVANCED_FACE('',(#1222),#1023,.F.);
#7328=CLOSED_SHELL('',(#6922,#6923,#6924,#6925,#6926,#6927));
#7966=AXIS2_PLACEMENT_3D('',#11508,#9054,#9055);
#7967=AXIS2_PLACEMENT_3D('',#11509,#9056,#9057);
#7968=AXIS2_PLACEMENT_3D('',#11518,#9062,#9063);
#7969=AXIS2_PLACEMENT_3D('',#11524,#9067,#9068);
#7970=AXIS2_PLACEMENT_3D('',#11530,#9072,#9073);
#7971=AXIS2_PLACEMENT_3D('',#11533,#9076,#9077);
#7972=AXIS2_PLACEMENT_3D('',#11534,#9078,#9079);
#9054=DIRECTION('axis',(0.,0.,1.));
#9055=DIRECTION('refdir',(1.,0.,0.));
#9056=DIRECTION('center_axis',(0.,1.,0.));
#9057=DIRECTION('ref_axis',(-1.,0.,0.));
#9058=DIRECTION('',(-1.,0.,0.));
#9059=DIRECTION('',(0.,0.,1.));
#9060=DIRECTION('',(-1.,0.,0.));
#9061=DIRECTION('',(0.,0.,1.));
#9062=DIRECTION('center_axis',(1.,0.,0.));
#9063=DIRECTION('ref_axis',(0.,1.,0.));
#9064=DIRECTION('',(0.,1.,0.));
#9065=DIRECTION('',(0.,1.,0.));
#9066=DIRECTION('',(0.,0.,1.));
#9067=DIRECTION('center_axis',(0.,-1.,0.));
#9068=DIRECTION('ref_axis',(1.,0.,0.));
#9069=DIRECTION('',(1.,0.,0.));
#9070=DIRECTION('',(1.,0.,0.));
#9071=DIRECTION('',(0.,0.,1.));
#9072=DIRECTION('center_axis',(-1.,0.,0.));
#9073=DIRECTION('ref_axis',(0.,-1.,0.));
#9074=DIRECTION('',(0.,-1.,0.));
#9075=DIRECTION('',(0.,-1.,0.));
#9076=DIRECTION('center_axis',(0.,0.,1.));
#9077=DIRECTION('ref_axis',(1.,0.,0.));
#9078=DIRECTION('center_axis',(0.,0.,1.));
#9079=DIRECTION('ref_axis',(1.,0.,0.));
#11508=CARTESIAN_POINT('',(0.,0.,0.));
#11509=CARTESIAN_POINT('Origin',(28.,10.,-0.5));
#11510=CARTESIAN_POINT('',(28.,10.,-0.5));
#11511=CARTESIAN_POINT('',(26.,10.,-0.5));
#11512=CARTESIAN_POINT('',(28.,10.,-0.5));
#11513=CARTESIAN_POINT('',(26.,10.,0.));
#11514=CARTESIAN_POINT('',(26.,10.,-0.5));
#11515=CARTESIAN_POINT('',(28.,10.,0.));
#11516=CARTESIAN_POINT('',(28.,10.,0.));
#11517=CARTESIAN_POINT('',(28.,10.,-0.5));
#11518=CARTESIAN_POINT('Origin',(28.,-5.,-0.5));
#11519=CARTESIAN_POINT('',(28.,-5.,-0.5));
#11520=CARTESIAN_POINT('',(28.,-5.,-0.5));
#11521=CARTESIAN_POINT('',(28.,-5.,0.));
#11522=CARTESIAN_POINT('',(28.,-5.,0.));
#11523=CARTESIAN_POINT('',(28.,-5.,-0.5));
#11524=CARTESIAN_POINT('Origin',(26.,-5.,-0.5));
#11525=CARTESIAN_POINT('',(26.,-5.,-0.5));
#11526=CARTESIAN_POINT('',(26.,-5.,-0.5));
#11527=CARTESIAN_POINT('',(26.,-5.,0.));
#11528=CARTESIAN_POINT('',(26.,-5.,0.));
#11529=CARTESIAN_POINT('',(26.,-5.,-0.5));
#11530=CARTESIAN_POINT('Origin',(26.,10.,-0.5));
#11531=CARTESIAN_POINT('',(26.,10.,-0.5));
#11532=CARTESIAN_POINT('',(26.,10.,0.));
#11533=CARTESIAN_POINT('Origin',(27.,2.5,0.));
#11534=CARTESIAN_POINT('Origin',(27.,2.5,-0.5));
#14403=UNCERTAINTY_MEASURE_WITH_UNIT(LENGTH_MEASURE(0.001),#14513,
'DISTANCE_ACCURACY_VALUE',
'Maximum model space distance between geometric entities at asserted c
onnectivities');
#14455=UNCERTAINTY_MEASURE_WITH_UNIT(LENGTH_MEASURE(0.001),#14513,
'DISTANCE_ACCURACY_VALUE',
'Maximum model space distance between geometric entities at asserted c
onnectivities');
#14460=(
GEOMETRIC_REPRESENTATION_CONTEXT(3)
GLOBAL_UNCERTAINTY_ASSIGNED_CONTEXT((#14403))
GLOBAL_UNIT_ASSIGNED_CONTEXT((#14513,#14515,#14516))
REPRESENTATION_CONTEXT('','3D')
);
#14512=(
GEOMETRIC_REPRESENTATION_CONTEXT(3)
GLOBAL_UNCERTAINTY_ASSIGNED_CONTEXT((#14455))
GLOBAL_UNIT_ASSIGNED_CONTEXT((#14513,#14515,#14516))
REPRESENTATION_CONTEXT('','3D')
);
#14513=(
LENGTH_UNIT()
NAMED_UNIT(*)
SI_UNIT(.CENTI.,.METRE.)
);
#14515=(
NAMED_UNIT(*)
PLANE_ANGLE_UNIT()
SI_UNIT($,.RADIAN.)
);
#14516=(
NAMED_UNIT(*)
SI_UNIT($,.STERADIAN.)
SOLID_ANGLE_UNIT()
);
#14521=SHAPE_DEFINITION_REPRESENTATION(#14577,#14745);
#14577=PRODUCT_DEFINITION_SHAPE('',$,#14802);
#14745=SHAPE_REPRESENTATION('',(#7966),#14460);
#14797=PRODUCT_DEFINITION_CONTEXT('part definition',#14967,'design');
#14802=PRODUCT_DEFINITION('Foot strip (1)','Foot strip (1)',#14858,#14797);
#14858=PRODUCT_DEFINITION_FORMATION('',$,#14973);
#14967=APPLICATION_CONTEXT(
'Core Data for Automotive Mechanical Design Process');
#14968=PRODUCT_CONTEXT('part definition',#14967,'mechanical');
#14973=PRODUCT('Foot strip (1)','Foot strip (1)','Foot strip (1)',(#14968));
#15067=COLOUR_RGB('Light Blue',0.38,0.62,0.78);
#15068=FILL_AREA_STYLE_COLOUR('',#15067);
#15069=FILL_AREA_STYLE('',(#15068));
#15070=SURFACE_STYLE_FILL_AREA(#15069);
#15071=SURFACE_SIDE_STYLE('',(#15070));
#15072=SURFACE_STYLE_USAGE(.BOTH.,#15071);
#15073=PRESENTATION_STYLE_ASSIGNMENT((#15072));
ENDSEC;
END-ISO-10303-21;
